ISO-10303-21;
HEADER;
FILE_DESCRIPTION (('STEP AP214'),
    '1' );
FILE_NAME ('plain washer clevis pin grade a_iso_ISO 8738 - 12.step',
    '2026-10-08T05:56:58',
    ( '' ),
    ( '' ),
    'SwSTEP 2.0',
    'SolidWorks 2026',
    '' );
FILE_SCHEMA (( 'AUTOMOTIVE_DESIGN' ));
ENDSEC;

DATA;
#93=EDGE_CURVE ( 'NONE', #2524, #1421, #17025, .T. ) ;
#122=CARTESIAN_POINT ( 'NONE',  ( -34.92499999999994742, 0.000000000000000000, 0.000000000000000000 ) ) ;
#268=( NAMED_UNIT ( * ) PLANE_ANGLE_UNIT ( ) SI_UNIT ( $, .RADIAN. ) );
#409=DIRECTION ( 'NONE',  ( -1.000000000000000000, -0.000000000000000000, -0.000000000000000000 ) ) ;
#466=FACE_BOUND ( 'NONE', #15200, .T. ) ;
#546=DIRECTION ( 'NONE',  ( -1.000000000000000000, -0.000000000000000000, -0.000000000000000000 ) ) ;
#646=FACE_OUTER_BOUND ( 'NONE', #17475, .T. ) ;
#780=DIRECTION ( 'NONE',  ( 0.000000000000000000, 0.000000000000000000, 1.000000000000000000 ) ) ;
#893=DIRECTION ( 'NONE',  ( 0.000000000000000000, 0.000000000000000000, 1.000000000000000000 ) ) ;
#904=ORIENTED_EDGE ( 'NONE', *, *, #7739, .T. ) ;
#911=EDGE_LOOP ( 'NONE', ( #2200, #15729 ) ) ;
#935=DIRECTION ( 'NONE',  ( 0.000000000000000000, 0.000000000000000000, 1.000000000000000000 ) ) ;
#1421=VERTEX_POINT ( 'NONE', #13774 ) ;
#1614=PRODUCT_DEFINITION ( 'UNKNOWN', '', #18501, #2773 ) ;
#1621=ADVANCED_FACE ( 'NONE', ( #15433 ), #13529, .T. ) ;
#1700=AXIS2_PLACEMENT_3D ( 'NONE', #5124, #546, #6518 ) ;
#1713=CIRCLE ( 'NONE', #6789, 10.00000000000000000 ) ;
#1743=DIRECTION ( 'NONE',  ( -1.000000000000000000, -0.000000000000000000, -0.000000000000000000 ) ) ;
#1938=ORIENTED_EDGE ( 'NONE', *, *, #17938, .F. ) ;
#1969=DIRECTION ( 'NONE',  ( -1.000000000000000000, -0.000000000000000000, -0.000000000000000000 ) ) ;
#1982=CARTESIAN_POINT ( 'NONE',  ( -34.92499999999994742, 0.000000000000000000, 10.00000000000000000 ) ) ;
#2200=ORIENTED_EDGE ( 'NONE', *, *, #19713, .T. ) ;
#2290=CYLINDRICAL_SURFACE ( 'NONE', #3298, 6.000000000000000000 ) ;
#2304=CIRCLE ( 'NONE', #13485, 10.00000000000000000 ) ;
#2333=DIRECTION ( 'NONE',  ( -1.000000000000000000, -0.000000000000000000, -0.000000000000000000 ) ) ;
#2475=SHAPE_REPRESENTATION ( 'plain washer clevis pin grade a_iso_ISO 8738 - 12', ( #16724 ), #17389 ) ;
#2477=DIRECTION ( 'NONE',  ( 0.000000000000000000, 0.000000000000000000, 1.000000000000000000 ) ) ;
#2524=VERTEX_POINT ( 'NONE', #8061 ) ;
#2572=DIRECTION ( 'NONE',  ( -0.000000000000000000, 0.000000000000000000, 1.000000000000000000 ) ) ;
#2666=PRODUCT ( 'plain washer clevis pin grade a_iso_ISO 8738 - 12', 'plain washer clevis pin grade a_iso_ISO 8738 - 12', '', ( #6332 ) ) ;
#2679=CARTESIAN_POINT ( 'NONE',  ( 0.000000000000000000, 0.000000000000000000, 0.000000000000000000 ) ) ;
#2693=SURFACE_STYLE_USAGE ( .BOTH. , #10220 ) ;
#2773=PRODUCT_DEFINITION_CONTEXT ( 'detailed design', #9450, 'design' ) ;
#3200=ADVANCED_FACE ( 'NONE', ( #10197, #15999 ), #13096, .F. ) ;
#3209=ADVANCED_FACE ( 'NONE', ( #8501 ), #2290, .F. ) ;
#3267=SHAPE_REPRESENTATION_RELATIONSHIP ( 'NONE' , 'NONE' ,  #2475, #7075 ) ;
#3298=AXIS2_PLACEMENT_3D ( 'NONE', #17503, #13196, #2477 ) ;
#3320=MECHANICAL_DESIGN_GEOMETRIC_PRESENTATION_REPRESENTATION('',(#8761),#10990);
#3347=ORIENTED_EDGE ( 'NONE', *, *, #7702, .F. ) ;
#3371=FILL_AREA_STYLE_COLOUR ( '', #3963 ) ;
#3749=ORIENTED_EDGE ( 'NONE', *, *, #8444, .F. ) ;
#3771=CARTESIAN_POINT ( 'NONE',  ( 0.000000000000000000, 0.000000000000000000, 0.000000000000000000 ) ) ;
#3788=EDGE_CURVE ( 'NONE', #8597, #10842, #12707, .T. ) ;
#3929=EDGE_CURVE ( 'NONE', #11356, #1421, #9718, .T. ) ;
#3963=COLOUR_RGB ( '', 0.40784314, 0.44705882, 0.49803922) ;
#4033=CYLINDRICAL_SURFACE ( 'NONE', #14237, 10.00000000000000000 ) ;
#4175=VECTOR ( 'NONE', #5077, 1000.000000000000000 ) ;
#4180=CARTESIAN_POINT ( 'NONE',  ( 0.000000000000000000, 7.347880794884119736E-16, -6.000000000000000000 ) ) ;
#4186=UNCERTAINTY_MEASURE_WITH_UNIT (LENGTH_MEASURE( 1.000000000000000082E-05 ), #14912, 'distance_accuracy_value', 'NONE');
#4378=ORIENTED_EDGE ( 'NONE', *, *, #12551, .F. ) ;
#4384=UNCERTAINTY_MEASURE_WITH_UNIT (LENGTH_MEASURE( 1.000000000000000082E-05 ), #6648, 'distance_accuracy_value', 'NONE');
#4706=DIRECTION ( 'NONE',  ( -1.000000000000000000, -0.000000000000000000, -0.000000000000000000 ) ) ;
#4714=ORIENTED_EDGE ( 'NONE', *, *, #5882, .T. ) ;
#4771=SURFACE_STYLE_FILL_AREA ( #9579 ) ;
#4775=ORIENTED_EDGE ( 'NONE', *, *, #8444, .T. ) ;
#5069=DIRECTION ( 'NONE',  ( -1.000000000000000000, -0.000000000000000000, -0.000000000000000000 ) ) ;
#5077=DIRECTION ( 'NONE',  ( -1.000000000000000000, -0.000000000000000000, -0.000000000000000000 ) ) ;
#5124=CARTESIAN_POINT ( 'NONE',  ( -3.000000000000002665, 0.000000000000000000, 0.000000000000000000 ) ) ;
#5125=MECHANICAL_DESIGN_GEOMETRIC_PRESENTATION_REPRESENTATION('',(#9616),#17920);
#5157=SURFACE_SIDE_STYLE ('',( #4771 ) ) ;
#5681=DIRECTION ( 'NONE',  ( -1.000000000000000000, -0.000000000000000000, -0.000000000000000000 ) ) ;
#5776=CARTESIAN_POINT ( 'NONE',  ( -34.92499999999994742, 0.000000000000000000, 0.000000000000000000 ) ) ;
#5882=EDGE_CURVE ( 'NONE', #17411, #2524, #9424, .T. ) ;
#5953=ORIENTED_EDGE ( 'NONE', *, *, #17613, .T. ) ;
#6230=DIRECTION ( 'NONE',  ( 1.000000000000000000, 0.000000000000000000, 0.000000000000000000 ) ) ;
#6332=PRODUCT_CONTEXT ( 'NONE', #19395, 'mechanical' ) ;
#6518=DIRECTION ( 'NONE',  ( 0.000000000000000000, 0.000000000000000000, 1.000000000000000000 ) ) ;
#6648=( LENGTH_UNIT ( ) NAMED_UNIT ( * ) SI_UNIT ( .MILLI., .METRE. ) );
#6789=AXIS2_PLACEMENT_3D ( 'NONE', #16361, #13263, #19353 ) ;
#6890=CARTESIAN_POINT ( 'NONE',  ( 0.000000000000000000, 0.000000000000000000, 6.000000000000000000 ) ) ;
#7063=CARTESIAN_POINT ( 'NONE',  ( 0.000000000000000000, 0.000000000000000000, 0.000000000000000000 ) ) ;
#7075=ADVANCED_BREP_SHAPE_REPRESENTATION ( '', ( #15810, #16724 ), #17389 ) ;
#7282=FILL_AREA_STYLE_COLOUR ( '', #16632 ) ;
#7425=CARTESIAN_POINT ( 'NONE',  ( -3.000000000000002665, 0.000000000000000000, 0.000000000000000000 ) ) ;
#7702=EDGE_CURVE ( 'NONE', #10842, #10348, #2304, .T. ) ;
#7739=EDGE_CURVE ( 'NONE', #8597, #9421, #17652, .T. ) ;
#7760=ORIENTED_EDGE ( 'NONE', *, *, #19713, .F. ) ;
#7771=ORIENTED_EDGE ( 'NONE', *, *, #17613, .F. ) ;
#7912=EDGE_LOOP ( 'NONE', ( #15261, #17283, #4714, #18710 ) ) ;
#7940=SHAPE_DEFINITION_REPRESENTATION ( #14506, #2475 ) ;
#8061=CARTESIAN_POINT ( 'NONE',  ( -3.000000000000002665, 0.000000000000000000, 6.000000000000000000 ) ) ;
#8357=EDGE_LOOP ( 'NONE', ( #18033, #19747, #7760, #7771 ) ) ;
#8444=EDGE_CURVE ( 'NONE', #11356, #17411, #13468, .T. ) ;
#8501=FACE_OUTER_BOUND ( 'NONE', #7912, .T. ) ;
#8556=ADVANCED_FACE ( 'NONE', ( #16501 ), #13203, .F. ) ;
#8597=VERTEX_POINT ( 'NONE', #15592 ) ;
#8761=STYLED_ITEM ( 'NONE', ( #17081 ), #7075 ) ;
#8790=CARTESIAN_POINT ( 'NONE',  ( 0.000000000000000000, 6.000000000000000000, 0.000000000000000000 ) ) ;
#8810=PRESENTATION_STYLE_ASSIGNMENT (( #2693 ) ) ;
#9187=ADVANCED_FACE ( 'NONE', ( #466, #11168 ), #15967, .F. ) ;
#9195=VECTOR ( 'NONE', #14103, 1000.000000000000000 ) ;
#9421=VERTEX_POINT ( 'NONE', #12444 ) ;
#9424=LINE ( 'NONE', #14111, #18091 ) ;
#9450=APPLICATION_CONTEXT ( 'automotive_design' ) ;
#9554=ORIENTED_EDGE ( 'NONE', *, *, #5882, .F. ) ;
#9570=DIRECTION ( 'NONE',  ( 1.000000000000000000, 0.000000000000000000, 0.000000000000000000 ) ) ;
#9579=FILL_AREA_STYLE ('',( #3371 ) ) ;
#9616=STYLED_ITEM ( 'NONE', ( #8810 ), #15810 ) ;
#9718=LINE ( 'NONE', #15611, #9195 ) ;
#9833=DIRECTION ( 'NONE',  ( 0.000000000000000000, 0.000000000000000000, 1.000000000000000000 ) ) ;
#10197=FACE_OUTER_BOUND ( 'NONE', #16017, .T. ) ;
#10209=EDGE_LOOP ( 'NONE', ( #3749, #10931, #15656, #9554 ) ) ;
#10220=SURFACE_SIDE_STYLE ('',( #19501 ) ) ;
#10348=VERTEX_POINT ( 'NONE', #12158 ) ;
#10404=DIRECTION ( 'NONE',  ( 0.000000000000000000, 0.000000000000000000, 1.000000000000000000 ) ) ;
#10415=FILL_AREA_STYLE ('',( #7282 ) ) ;
#10730=DIRECTION ( 'NONE',  ( 0.000000000000000000, 0.000000000000000000, 1.000000000000000000 ) ) ;
#10842=VERTEX_POINT ( 'NONE', #19019 ) ;
#10878=( NAMED_UNIT ( * ) SI_UNIT ( $, .STERADIAN. ) SOLID_ANGLE_UNIT ( ) );
#10931=ORIENTED_EDGE ( 'NONE', *, *, #3929, .T. ) ;
#10990=( GEOMETRIC_REPRESENTATION_CONTEXT ( 3 ) GLOBAL_UNCERTAINTY_ASSIGNED_CONTEXT ( ( #13197 ) ) GLOBAL_UNIT_ASSIGNED_CONTEXT ( ( #14070, #268, #10878 ) ) REPRESENTATION_CONTEXT ( 'NONE', 'WORKASPACE' ) );
#11168=FACE_OUTER_BOUND ( 'NONE', #911, .T. ) ;
#11276=( NAMED_UNIT ( * ) PLANE_ANGLE_UNIT ( ) SI_UNIT ( $, .RADIAN. ) );
#11356=VERTEX_POINT ( 'NONE', #4180 ) ;
#11552=AXIS2_PLACEMENT_3D ( 'NONE', #7425, #1743, #16763 ) ;
#11846=AXIS2_PLACEMENT_3D ( 'NONE', #16870, #13862, #12164 ) ;
#12011=( NAMED_UNIT ( * ) PLANE_ANGLE_UNIT ( ) SI_UNIT ( $, .RADIAN. ) );
#12158=CARTESIAN_POINT ( 'NONE',  ( -3.000000000000002665, 0.000000000000000000, 10.00000000000000000 ) ) ;
#12164=DIRECTION ( 'NONE',  ( 0.000000000000000000, 0.000000000000000000, 1.000000000000000000 ) ) ;
#12406=CIRCLE ( 'NONE', #14955, 10.00000000000000000 ) ;
#12415=CARTESIAN_POINT ( 'NONE',  ( -34.92499999999994742, 1.224646799147353256E-15, -10.00000000000000000 ) ) ;
#12444=CARTESIAN_POINT ( 'NONE',  ( 0.000000000000000000, 0.000000000000000000, 10.00000000000000000 ) ) ;
#12551=EDGE_CURVE ( 'NONE', #9421, #8597, #12406, .T. ) ;
#12576=AXIS2_PLACEMENT_3D ( 'NONE', #8790, #16296, #2572 ) ;
#12707=LINE ( 'NONE', #12415, #14612 ) ;
#13096=PLANE ( 'NONE',  #12576 ) ;
#13196=DIRECTION ( 'NONE',  ( -1.000000000000000000, -0.000000000000000000, -0.000000000000000000 ) ) ;
#13197=UNCERTAINTY_MEASURE_WITH_UNIT (LENGTH_MEASURE( 1.000000000000000082E-05 ), #14070, 'distance_accuracy_value', 'NONE');
#13203=CYLINDRICAL_SURFACE ( 'NONE', #14114, 6.000000000000000000 ) ;
#13263=DIRECTION ( 'NONE',  ( -1.000000000000000000, -0.000000000000000000, -0.000000000000000000 ) ) ;
#13468=CIRCLE ( 'NONE', #15079, 6.000000000000000000 ) ;
#13485=AXIS2_PLACEMENT_3D ( 'NONE', #17384, #5069, #780 ) ;
#13497=AXIS2_PLACEMENT_3D ( 'NONE', #14471, #9570, #17172 ) ;
#13529=CYLINDRICAL_SURFACE ( 'NONE', #14523, 10.00000000000000000 ) ;
#13774=CARTESIAN_POINT ( 'NONE',  ( -3.000000000000002665, 7.347880794884119736E-16, -6.000000000000000000 ) ) ;
#13862=DIRECTION ( 'NONE',  ( -1.000000000000000000, -0.000000000000000000, -0.000000000000000000 ) ) ;
#14070=( LENGTH_UNIT ( ) NAMED_UNIT ( * ) SI_UNIT ( .MILLI., .METRE. ) );
#14103=DIRECTION ( 'NONE',  ( -1.000000000000000000, -0.000000000000000000, -0.000000000000000000 ) ) ;
#14111=CARTESIAN_POINT ( 'NONE',  ( -34.92499999999994742, 0.000000000000000000, 6.000000000000000000 ) ) ;
#14114=AXIS2_PLACEMENT_3D ( 'NONE', #5776, #19692, #17803 ) ;
#14237=AXIS2_PLACEMENT_3D ( 'NONE', #19139, #2333, #935 ) ;
#14242=ADVANCED_FACE ( 'NONE', ( #646 ), #4033, .T. ) ;
#14322=ORIENTED_EDGE ( 'NONE', *, *, #3788, .F. ) ;
#14471=CARTESIAN_POINT ( 'NONE',  ( -3.000000000000001332, 10.00000000000000000, 0.000000000000000000 ) ) ;
#14488=EDGE_LOOP ( 'NONE', ( #17582, #4775 ) ) ;
#14506=PRODUCT_DEFINITION_SHAPE ( 'NONE', 'NONE',  #1614 ) ;
#14523=AXIS2_PLACEMENT_3D ( 'NONE', #122, #15034, #10730 ) ;
#14612=VECTOR ( 'NONE', #4706, 1000.000000000000000 ) ;
#14912=( LENGTH_UNIT ( ) NAMED_UNIT ( * ) SI_UNIT ( .MILLI., .METRE. ) );
#14955=AXIS2_PLACEMENT_3D ( 'NONE', #7063, #15998, #893 ) ;
#15034=DIRECTION ( 'NONE',  ( -1.000000000000000000, -0.000000000000000000, -0.000000000000000000 ) ) ;
#15079=AXIS2_PLACEMENT_3D ( 'NONE', #2679, #5681, #10404 ) ;
#15200=EDGE_LOOP ( 'NONE', ( #19053, #1938 ) ) ;
#15261=ORIENTED_EDGE ( 'NONE', *, *, #3929, .F. ) ;
#15433=FACE_OUTER_BOUND ( 'NONE', #8357, .T. ) ;
#15592=CARTESIAN_POINT ( 'NONE',  ( 0.000000000000000000, 1.224646799147353256E-15, -10.00000000000000000 ) ) ;
#15611=CARTESIAN_POINT ( 'NONE',  ( -34.92499999999994742, 7.347880794884119736E-16, -6.000000000000000000 ) ) ;
#15656=ORIENTED_EDGE ( 'NONE', *, *, #17938, .T. ) ;
#15692=LINE ( 'NONE', #1982, #4175 ) ;
#15729=ORIENTED_EDGE ( 'NONE', *, *, #7702, .T. ) ;
#15810=MANIFOLD_SOLID_BREP ( 'Base-Revolve', #18000 ) ;
#15967=PLANE ( 'NONE',  #13497 ) ;
#15998=DIRECTION ( 'NONE',  ( -1.000000000000000000, -0.000000000000000000, -0.000000000000000000 ) ) ;
#15999=FACE_BOUND ( 'NONE', #14488, .T. ) ;
#16017=EDGE_LOOP ( 'NONE', ( #4378, #18285 ) ) ;
#16051=EDGE_CURVE ( 'NONE', #17411, #11356, #18517, .T. ) ;
#16296=DIRECTION ( 'NONE',  ( -1.000000000000000000, 0.000000000000000000, -0.000000000000000000 ) ) ;
#16361=CARTESIAN_POINT ( 'NONE',  ( -3.000000000000002665, 0.000000000000000000, 0.000000000000000000 ) ) ;
#16501=FACE_OUTER_BOUND ( 'NONE', #10209, .T. ) ;
#16632=COLOUR_RGB ( '', 0.40784314, 0.44705882, 0.49803922) ;
#16661=CIRCLE ( 'NONE', #11552, 6.000000000000000000 ) ;
#16724=AXIS2_PLACEMENT_3D ( 'NONE', #17428, #9833, #6230 ) ;
#16763=DIRECTION ( 'NONE',  ( 0.000000000000000000, 0.000000000000000000, 1.000000000000000000 ) ) ;
#16870=CARTESIAN_POINT ( 'NONE',  ( 0.000000000000000000, 0.000000000000000000, 0.000000000000000000 ) ) ;
#17025=CIRCLE ( 'NONE', #1700, 6.000000000000000000 ) ;
#17081=PRESENTATION_STYLE_ASSIGNMENT (( #18873 ) ) ;
#17172=DIRECTION ( 'NONE',  ( 0.000000000000000000, 0.000000000000000000, -1.000000000000000000 ) ) ;
#17274=( NAMED_UNIT ( * ) SI_UNIT ( $, .STERADIAN. ) SOLID_ANGLE_UNIT ( ) );
#17282=DIRECTION ( 'NONE',  ( 0.000000000000000000, 0.000000000000000000, 1.000000000000000000 ) ) ;
#17283=ORIENTED_EDGE ( 'NONE', *, *, #16051, .F. ) ;
#17384=CARTESIAN_POINT ( 'NONE',  ( -3.000000000000002665, 0.000000000000000000, 0.000000000000000000 ) ) ;
#17389=( GEOMETRIC_REPRESENTATION_CONTEXT ( 3 ) GLOBAL_UNCERTAINTY_ASSIGNED_CONTEXT ( ( #4384 ) ) GLOBAL_UNIT_ASSIGNED_CONTEXT ( ( #6648, #11276, #17274 ) ) REPRESENTATION_CONTEXT ( 'NONE', 'WORKASPACE' ) );
#17411=VERTEX_POINT ( 'NONE', #6890 ) ;
#17428=CARTESIAN_POINT ( 'NONE',  ( 0.000000000000000000, 0.000000000000000000, 0.000000000000000000 ) ) ;
#17475=EDGE_LOOP ( 'NONE', ( #14322, #904, #5953, #3347 ) ) ;
#17503=CARTESIAN_POINT ( 'NONE',  ( -34.92499999999994742, 0.000000000000000000, 0.000000000000000000 ) ) ;
#17582=ORIENTED_EDGE ( 'NONE', *, *, #16051, .T. ) ;
#17613=EDGE_CURVE ( 'NONE', #9421, #10348, #15692, .T. ) ;
#17618=AXIS2_PLACEMENT_3D ( 'NONE', #3771, #1969, #17282 ) ;
#17652=CIRCLE ( 'NONE', #17618, 10.00000000000000000 ) ;
#17803=DIRECTION ( 'NONE',  ( 0.000000000000000000, 0.000000000000000000, 1.000000000000000000 ) ) ;
#17817=( NAMED_UNIT ( * ) SI_UNIT ( $, .STERADIAN. ) SOLID_ANGLE_UNIT ( ) );
#17920=( GEOMETRIC_REPRESENTATION_CONTEXT ( 3 ) GLOBAL_UNCERTAINTY_ASSIGNED_CONTEXT ( ( #4186 ) ) GLOBAL_UNIT_ASSIGNED_CONTEXT ( ( #14912, #12011, #17817 ) ) REPRESENTATION_CONTEXT ( 'NONE', 'WORKASPACE' ) );
#17938=EDGE_CURVE ( 'NONE', #1421, #2524, #16661, .T. ) ;
#18000=CLOSED_SHELL ( 'NONE', ( #1621, #8556, #3209, #3200, #14242, #9187 ) ) ;
#18033=ORIENTED_EDGE ( 'NONE', *, *, #12551, .T. ) ;
#18091=VECTOR ( 'NONE', #409, 1000.000000000000000 ) ;
#18285=ORIENTED_EDGE ( 'NONE', *, *, #7739, .F. ) ;
#18501=PRODUCT_DEFINITION_FORMATION_WITH_SPECIFIED_SOURCE ( 'ANY', '', #2666, .NOT_KNOWN. ) ;
#18517=CIRCLE ( 'NONE', #11846, 6.000000000000000000 ) ;
#18710=ORIENTED_EDGE ( 'NONE', *, *, #93, .T. ) ;
#18873=SURFACE_STYLE_USAGE ( .BOTH. , #5157 ) ;
#19019=CARTESIAN_POINT ( 'NONE',  ( -3.000000000000002665, 1.224646799147353256E-15, -10.00000000000000000 ) ) ;
#19053=ORIENTED_EDGE ( 'NONE', *, *, #93, .F. ) ;
#19139=CARTESIAN_POINT ( 'NONE',  ( -34.92499999999994742, 0.000000000000000000, 0.000000000000000000 ) ) ;
#19353=DIRECTION ( 'NONE',  ( 0.000000000000000000, 0.000000000000000000, 1.000000000000000000 ) ) ;
#19395=APPLICATION_CONTEXT ( 'automotive_design' ) ;
#19501=SURFACE_STYLE_FILL_AREA ( #10415 ) ;
#19692=DIRECTION ( 'NONE',  ( -1.000000000000000000, -0.000000000000000000, -0.000000000000000000 ) ) ;
#19713=EDGE_CURVE ( 'NONE', #10348, #10842, #1713, .T. ) ;
#19747=ORIENTED_EDGE ( 'NONE', *, *, #3788, .T. ) ;
ENDSEC;
END-ISO-10303-21;
